ISO-10303-21;
HEADER;
/* Generated by software containing ST-Developer
 * from STEP Tools, Inc. (www.steptools.com) 
 */

FILE_DESCRIPTION(
/* description */ ('V-block with clamp strap'),
/* implementation_level */ '2;1');

FILE_NAME(
/* name */ 'M4x10 Cap Screw.step',
/* time_stamp */ '2026-10-27T10:50:53-07:00',
/* author */ (''),
/* organization */ (''),
/* preprocessor_version */ 'ST-DEVELOPER v20.2',
/* originating_system */ 'Autodesk Translation Framework v15.17.0.0',
/* authorisation */ '');

FILE_SCHEMA (('AUTOMOTIVE_DESIGN { 1 0 10303 214 3 1 1 }'));
ENDSEC;

DATA;
#10=MECHANICAL_DESIGN_GEOMETRIC_PRESENTATION_REPRESENTATION('',(#283),#7344);
#201=ORIENTED_CLOSED_SHELL('',*,#4167,.F.);
#212=CONICAL_SURFACE('',#4782,0.325,0.785398163397448);
#213=CONICAL_SURFACE('',#4786,0.335,0.785398163397448);
#214=CONICAL_SURFACE('',#4790,0.21,0.463647609000806);
#219=BREP_WITH_VOIDS('Body1',#4168,(#201));
#241=SHAPE_REPRESENTATION_RELATIONSHIP('SRR','None',#7460,#262);
#262=ADVANCED_BREP_SHAPE_REPRESENTATION('',(#219),#7339);
#283=STYLED_ITEM('',(#7638),#219);
#371=FACE_BOUND('',#1088,.T.);
#488=CIRCLE('',#4779,0.1954);
#489=CIRCLE('',#4781,0.3);
#490=CIRCLE('',#4783,0.35);
#491=CIRCLE('',#4785,0.35);
#492=CIRCLE('',#4787,0.32);
#493=CIRCLE('',#4789,0.22);
#494=CIRCLE('',#4791,0.1954);
#556=CYLINDRICAL_SURFACE('',#4784,0.35);
#557=CYLINDRICAL_SURFACE('',#4792,0.1954);
#768=FACE_OUTER_BOUND('',#1074,.T.);
#769=FACE_OUTER_BOUND('',#1075,.T.);
#770=FACE_OUTER_BOUND('',#1076,.T.);
#771=FACE_OUTER_BOUND('',#1077,.T.);
#772=FACE_OUTER_BOUND('',#1078,.T.);
#773=FACE_OUTER_BOUND('',#1079,.T.);
#774=FACE_OUTER_BOUND('',#1080,.T.);
#775=FACE_OUTER_BOUND('',#1081,.T.);
#776=FACE_OUTER_BOUND('',#1082,.T.);
#777=FACE_OUTER_BOUND('',#1083,.T.);
#778=FACE_OUTER_BOUND('',#1084,.T.);
#779=FACE_OUTER_BOUND('',#1085,.T.);
#780=FACE_OUTER_BOUND('',#1086,.T.);
#781=FACE_OUTER_BOUND('',#1087,.T.);
#782=FACE_OUTER_BOUND('',#1089,.T.);
#783=FACE_OUTER_BOUND('',#1090,.T.);
#1074=EDGE_LOOP('',(#3612,#3613,#3614,#3615));
#1075=EDGE_LOOP('',(#3616,#3617,#3618,#3619));
#1076=EDGE_LOOP('',(#3620,#3621,#3622,#3623));
#1077=EDGE_LOOP('',(#3624,#3625,#3626,#3627));
#1078=EDGE_LOOP('',(#3628,#3629,#3630,#3631));
#1079=EDGE_LOOP('',(#3632,#3633,#3634,#3635));
#1080=EDGE_LOOP('',(#3636,#3637,#3638,#3639,#3640,#3641));
#1081=EDGE_LOOP('',(#3642,#3643,#3644,#3645,#3646,#3647));
#1082=EDGE_LOOP('',(#3648));
#1083=EDGE_LOOP('',(#3649));
#1084=EDGE_LOOP('',(#3650,#3651,#3652,#3653));
#1085=EDGE_LOOP('',(#3654,#3655,#3656,#3657));
#1086=EDGE_LOOP('',(#3658,#3659,#3660,#3661));
#1087=EDGE_LOOP('',(#3662));
#1088=EDGE_LOOP('',(#3663));
#1089=EDGE_LOOP('',(#3664,#3665,#3666,#3667));
#1090=EDGE_LOOP('',(#3668,#3669,#3670,#3671));
#1443=LINE('',#7111,#1808);
#1444=LINE('',#7113,#1809);
#1445=LINE('',#7115,#1810);
#1446=LINE('',#7116,#1811);
#1447=LINE('',#7119,#1812);
#1448=LINE('',#7121,#1813);
#1449=LINE('',#7122,#1814);
#1450=LINE('',#7125,#1815);
#1451=LINE('',#7127,#1816);
#1452=LINE('',#7128,#1817);
#1453=LINE('',#7131,#1818);
#1454=LINE('',#7133,#1819);
#1455=LINE('',#7134,#1820);
#1456=LINE('',#7137,#1821);
#1457=LINE('',#7139,#1822);
#1458=LINE('',#7140,#1823);
#1459=LINE('',#7142,#1824);
#1460=LINE('',#7143,#1825);
#1461=LINE('',#7155,#1826);
#1462=LINE('',#7159,#1827);
#1463=LINE('',#7163,#1828);
#1464=LINE('',#7170,#1829);
#1465=LINE('',#7172,#1830);
#1808=VECTOR('',#5907,1.);
#1809=VECTOR('',#5908,1.);
#1810=VECTOR('',#5909,1.);
#1811=VECTOR('',#5910,1.);
#1812=VECTOR('',#5913,1.);
#1813=VECTOR('',#5914,1.);
#1814=VECTOR('',#5915,1.);
#1815=VECTOR('',#5918,1.);
#1816=VECTOR('',#5919,1.);
#1817=VECTOR('',#5920,1.);
#1818=VECTOR('',#5923,1.);
#1819=VECTOR('',#5924,1.);
#1820=VECTOR('',#5925,1.);
#1821=VECTOR('',#5928,1.);
#1822=VECTOR('',#5929,1.);
#1823=VECTOR('',#5930,1.);
#1824=VECTOR('',#5933,1.);
#1825=VECTOR('',#5934,1.);
#1826=VECTOR('',#5951,0.325);
#1827=VECTOR('',#5956,0.35);
#1828=VECTOR('',#5961,0.335);
#1829=VECTOR('',#5970,0.21);
#1830=VECTOR('',#5973,0.2);
#2133=VERTEX_POINT('',#7109);
#2134=VERTEX_POINT('',#7110);
#2135=VERTEX_POINT('',#7112);
#2136=VERTEX_POINT('',#7114);
#2137=VERTEX_POINT('',#7118);
#2138=VERTEX_POINT('',#7120);
#2139=VERTEX_POINT('',#7124);
#2140=VERTEX_POINT('',#7126);
#2141=VERTEX_POINT('',#7130);
#2142=VERTEX_POINT('',#7132);
#2143=VERTEX_POINT('',#7136);
#2144=VERTEX_POINT('',#7138);
#2145=VERTEX_POINT('',#7147);
#2146=VERTEX_POINT('',#7150);
#2147=VERTEX_POINT('',#7153);
#2148=VERTEX_POINT('',#7157);
#2149=VERTEX_POINT('',#7161);
#2150=VERTEX_POINT('',#7165);
#2151=VERTEX_POINT('',#7168);
#2632=EDGE_CURVE('',#2133,#2134,#1443,.T.);
#2633=EDGE_CURVE('',#2134,#2135,#1444,.T.);
#2634=EDGE_CURVE('',#2135,#2136,#1445,.T.);
#2635=EDGE_CURVE('',#2133,#2136,#1446,.T.);
#2636=EDGE_CURVE('',#2134,#2137,#1447,.T.);
#2637=EDGE_CURVE('',#2137,#2138,#1448,.T.);
#2638=EDGE_CURVE('',#2138,#2135,#1449,.T.);
#2639=EDGE_CURVE('',#2137,#2139,#1450,.T.);
#2640=EDGE_CURVE('',#2139,#2140,#1451,.T.);
#2641=EDGE_CURVE('',#2140,#2138,#1452,.T.);
#2642=EDGE_CURVE('',#2139,#2141,#1453,.T.);
#2643=EDGE_CURVE('',#2141,#2142,#1454,.T.);
#2644=EDGE_CURVE('',#2142,#2140,#1455,.T.);
#2645=EDGE_CURVE('',#2141,#2143,#1456,.T.);
#2646=EDGE_CURVE('',#2143,#2144,#1457,.T.);
#2647=EDGE_CURVE('',#2144,#2142,#1458,.T.);
#2648=EDGE_CURVE('',#2143,#2133,#1459,.T.);
#2649=EDGE_CURVE('',#2136,#2144,#1460,.T.);
#2650=EDGE_CURVE('',#2145,#2145,#488,.T.);
#2651=EDGE_CURVE('',#2146,#2146,#489,.T.);
#2652=EDGE_CURVE('',#2147,#2147,#490,.T.);
#2653=EDGE_CURVE('',#2147,#2146,#1461,.T.);
#2654=EDGE_CURVE('',#2148,#2148,#491,.T.);
#2655=EDGE_CURVE('',#2148,#2147,#1462,.T.);
#2656=EDGE_CURVE('',#2149,#2149,#492,.T.);
#2657=EDGE_CURVE('',#2149,#2148,#1463,.T.);
#2658=EDGE_CURVE('',#2150,#2150,#493,.T.);
#2659=EDGE_CURVE('',#2151,#2151,#494,.F.);
#2660=EDGE_CURVE('',#2151,#2150,#1464,.T.);
#2661=EDGE_CURVE('',#2145,#2151,#1465,.T.);
#3612=ORIENTED_EDGE('',*,*,#2632,.T.);
#3613=ORIENTED_EDGE('',*,*,#2633,.T.);
#3614=ORIENTED_EDGE('',*,*,#2634,.T.);
#3615=ORIENTED_EDGE('',*,*,#2635,.F.);
#3616=ORIENTED_EDGE('',*,*,#2636,.T.);
#3617=ORIENTED_EDGE('',*,*,#2637,.T.);
#3618=ORIENTED_EDGE('',*,*,#2638,.T.);
#3619=ORIENTED_EDGE('',*,*,#2633,.F.);
#3620=ORIENTED_EDGE('',*,*,#2639,.T.);
#3621=ORIENTED_EDGE('',*,*,#2640,.T.);
#3622=ORIENTED_EDGE('',*,*,#2641,.T.);
#3623=ORIENTED_EDGE('',*,*,#2637,.F.);
#3624=ORIENTED_EDGE('',*,*,#2642,.T.);
#3625=ORIENTED_EDGE('',*,*,#2643,.T.);
#3626=ORIENTED_EDGE('',*,*,#2644,.T.);
#3627=ORIENTED_EDGE('',*,*,#2640,.F.);
#3628=ORIENTED_EDGE('',*,*,#2645,.T.);
#3629=ORIENTED_EDGE('',*,*,#2646,.T.);
#3630=ORIENTED_EDGE('',*,*,#2647,.T.);
#3631=ORIENTED_EDGE('',*,*,#2643,.F.);
#3632=ORIENTED_EDGE('',*,*,#2648,.T.);
#3633=ORIENTED_EDGE('',*,*,#2635,.T.);
#3634=ORIENTED_EDGE('',*,*,#2649,.T.);
#3635=ORIENTED_EDGE('',*,*,#2646,.F.);
#3636=ORIENTED_EDGE('',*,*,#2648,.F.);
#3637=ORIENTED_EDGE('',*,*,#2645,.F.);
#3638=ORIENTED_EDGE('',*,*,#2642,.F.);
#3639=ORIENTED_EDGE('',*,*,#2639,.F.);
#3640=ORIENTED_EDGE('',*,*,#2636,.F.);
#3641=ORIENTED_EDGE('',*,*,#2632,.F.);
#3642=ORIENTED_EDGE('',*,*,#2649,.F.);
#3643=ORIENTED_EDGE('',*,*,#2634,.F.);
#3644=ORIENTED_EDGE('',*,*,#2638,.F.);
#3645=ORIENTED_EDGE('',*,*,#2641,.F.);
#3646=ORIENTED_EDGE('',*,*,#2644,.F.);
#3647=ORIENTED_EDGE('',*,*,#2647,.F.);
#3648=ORIENTED_EDGE('',*,*,#2650,.F.);
#3649=ORIENTED_EDGE('',*,*,#2651,.F.);
#3650=ORIENTED_EDGE('',*,*,#2652,.F.);
#3651=ORIENTED_EDGE('',*,*,#2653,.T.);
#3652=ORIENTED_EDGE('',*,*,#2651,.T.);
#3653=ORIENTED_EDGE('',*,*,#2653,.F.);
#3654=ORIENTED_EDGE('',*,*,#2654,.F.);
#3655=ORIENTED_EDGE('',*,*,#2655,.T.);
#3656=ORIENTED_EDGE('',*,*,#2652,.T.);
#3657=ORIENTED_EDGE('',*,*,#2655,.F.);
#3658=ORIENTED_EDGE('',*,*,#2656,.F.);
#3659=ORIENTED_EDGE('',*,*,#2657,.T.);
#3660=ORIENTED_EDGE('',*,*,#2654,.T.);
#3661=ORIENTED_EDGE('',*,*,#2657,.F.);
#3662=ORIENTED_EDGE('',*,*,#2656,.T.);
#3663=ORIENTED_EDGE('',*,*,#2658,.F.);
#3664=ORIENTED_EDGE('',*,*,#2659,.F.);
#3665=ORIENTED_EDGE('',*,*,#2660,.T.);
#3666=ORIENTED_EDGE('',*,*,#2658,.T.);
#3667=ORIENTED_EDGE('',*,*,#2660,.F.);
#3668=ORIENTED_EDGE('',*,*,#2650,.T.);
#3669=ORIENTED_EDGE('',*,*,#2661,.T.);
#3670=ORIENTED_EDGE('',*,*,#2659,.T.);
#3671=ORIENTED_EDGE('',*,*,#2661,.F.);
#3885=PLANE('',#4770);
#3886=PLANE('',#4771);
#3887=PLANE('',#4772);
#3888=PLANE('',#4773);
#3889=PLANE('',#4774);
#3890=PLANE('',#4775);
#3891=PLANE('',#4776);
#3892=PLANE('',#4777);
#3893=PLANE('',#4778);
#3894=PLANE('',#4780);
#3895=PLANE('',#4788);
#4114=ADVANCED_FACE('',(#768),#3885,.F.);
#4115=ADVANCED_FACE('',(#769),#3886,.F.);
#4116=ADVANCED_FACE('',(#770),#3887,.F.);
#4117=ADVANCED_FACE('',(#771),#3888,.F.);
#4118=ADVANCED_FACE('',(#772),#3889,.F.);
#4119=ADVANCED_FACE('',(#773),#3890,.F.);
#4120=ADVANCED_FACE('',(#774),#3891,.F.);
#4121=ADVANCED_FACE('',(#775),#3892,.F.);
#4122=ADVANCED_FACE('',(#776),#3893,.F.);
#4123=ADVANCED_FACE('',(#777),#3894,.T.);
#4124=ADVANCED_FACE('',(#778),#212,.T.);
#4125=ADVANCED_FACE('',(#779),#556,.T.);
#4126=ADVANCED_FACE('',(#780),#213,.T.);
#4127=ADVANCED_FACE('',(#781,#371),#3895,.T.);
#4128=ADVANCED_FACE('',(#782),#214,.T.);
#4129=ADVANCED_FACE('',(#783),#557,.T.);
#4167=CLOSED_SHELL('',(#4114,#4115,#4116,#4117,#4118,#4119,#4120,#4121));
#4168=CLOSED_SHELL('',(#4122,#4123,#4124,#4125,#4126,#4127,#4128,#4129));
#4769=AXIS2_PLACEMENT_3D('',#7107,#5903,#5904);
#4770=AXIS2_PLACEMENT_3D('',#7108,#5905,#5906);
#4771=AXIS2_PLACEMENT_3D('',#7117,#5911,#5912);
#4772=AXIS2_PLACEMENT_3D('',#7123,#5916,#5917);
#4773=AXIS2_PLACEMENT_3D('',#7129,#5921,#5922);
#4774=AXIS2_PLACEMENT_3D('',#7135,#5926,#5927);
#4775=AXIS2_PLACEMENT_3D('',#7141,#5931,#5932);
#4776=AXIS2_PLACEMENT_3D('',#7144,#5935,#5936);
#4777=AXIS2_PLACEMENT_3D('',#7145,#5937,#5938);
#4778=AXIS2_PLACEMENT_3D('',#7146,#5939,#5940);
#4779=AXIS2_PLACEMENT_3D('',#7148,#5941,#5942);
#4780=AXIS2_PLACEMENT_3D('',#7149,#5943,#5944);
#4781=AXIS2_PLACEMENT_3D('',#7151,#5945,#5946);
#4782=AXIS2_PLACEMENT_3D('',#7152,#5947,#5948);
#4783=AXIS2_PLACEMENT_3D('',#7154,#5949,#5950);
#4784=AXIS2_PLACEMENT_3D('',#7156,#5952,#5953);
#4785=AXIS2_PLACEMENT_3D('',#7158,#5954,#5955);
#4786=AXIS2_PLACEMENT_3D('',#7160,#5957,#5958);
#4787=AXIS2_PLACEMENT_3D('',#7162,#5959,#5960);
#4788=AXIS2_PLACEMENT_3D('',#7164,#5962,#5963);
#4789=AXIS2_PLACEMENT_3D('',#7166,#5964,#5965);
#4790=AXIS2_PLACEMENT_3D('',#7167,#5966,#5967);
#4791=AXIS2_PLACEMENT_3D('',#7169,#5968,#5969);
#4792=AXIS2_PLACEMENT_3D('',#7171,#5971,#5972);
#5903=DIRECTION('axis',(0.,0.,1.));
#5904=DIRECTION('refdir',(1.,0.,0.));
#5905=DIRECTION('center_axis',(0.866025403784439,0.,-0.5));
#5906=DIRECTION('ref_axis',(0.5,0.,0.866025403784439));
#5907=DIRECTION('',(-0.5,0.,-0.866025403784439));
#5908=DIRECTION('',(0.,-1.,0.));
#5909=DIRECTION('',(0.5,0.,0.866025403784439));
#5910=DIRECTION('',(0.,-1.,0.));
#5911=DIRECTION('center_axis',(1.60246890531964E-16,0.,-1.));
#5912=DIRECTION('ref_axis',(1.,0.,1.60246890531964E-16));
#5913=DIRECTION('',(-1.,0.,-1.60246890531964E-16));
#5914=DIRECTION('',(0.,-1.,0.));
#5915=DIRECTION('',(1.,0.,1.60246890531964E-16));
#5916=DIRECTION('center_axis',(-0.866025403784439,0.,-0.5));
#5917=DIRECTION('ref_axis',(0.5,0.,-0.866025403784439));
#5918=DIRECTION('',(-0.5,0.,0.866025403784439));
#5919=DIRECTION('',(0.,-1.,0.));
#5920=DIRECTION('',(0.5,0.,-0.866025403784439));
#5921=DIRECTION('center_axis',(-0.866025403784439,0.,0.5));
#5922=DIRECTION('ref_axis',(-0.5,0.,-0.866025403784439));
#5923=DIRECTION('',(0.5,0.,0.866025403784439));
#5924=DIRECTION('',(0.,-1.,0.));
#5925=DIRECTION('',(-0.5,0.,-0.866025403784439));
#5926=DIRECTION('center_axis',(-1.60246890531964E-16,0.,1.));
#5927=DIRECTION('ref_axis',(-1.,0.,-1.60246890531964E-16));
#5928=DIRECTION('',(1.,0.,1.60246890531964E-16));
#5929=DIRECTION('',(0.,-1.,0.));
#5930=DIRECTION('',(-1.,0.,-1.60246890531964E-16));
#5931=DIRECTION('center_axis',(0.866025403784439,0.,0.5));
#5932=DIRECTION('ref_axis',(-0.5,0.,0.866025403784439));
#5933=DIRECTION('',(0.5,0.,-0.866025403784439));
#5934=DIRECTION('',(-0.5,0.,0.866025403784439));
#5935=DIRECTION('center_axis',(0.,1.,0.));
#5936=DIRECTION('ref_axis',(1.,0.,0.));
#5937=DIRECTION('center_axis',(0.,-1.,0.));
#5938=DIRECTION('ref_axis',(0.,0.,-1.));
#5939=DIRECTION('center_axis',(0.,1.,0.));
#5940=DIRECTION('ref_axis',(1.,0.,0.));
#5941=DIRECTION('center_axis',(0.,1.,0.));
#5942=DIRECTION('ref_axis',(1.,0.,0.));
#5943=DIRECTION('center_axis',(0.,1.,0.));
#5944=DIRECTION('ref_axis',(0.,0.,1.));
#5945=DIRECTION('center_axis',(0.,-1.,0.));
#5946=DIRECTION('ref_axis',(1.,0.,0.));
#5947=DIRECTION('center_axis',(0.,-1.,0.));
#5948=DIRECTION('ref_axis',(1.,0.,0.));
#5949=DIRECTION('center_axis',(0.,-1.,0.));
#5950=DIRECTION('ref_axis',(1.,0.,0.));
#5951=DIRECTION('',(0.707106781186547,0.707106781186548,8.65956056235493E-17));
#5952=DIRECTION('center_axis',(0.,-1.,0.));
#5953=DIRECTION('ref_axis',(1.,0.,0.));
#5954=DIRECTION('center_axis',(0.,-1.,0.));
#5955=DIRECTION('ref_axis',(1.,0.,0.));
#5956=DIRECTION('',(0.,1.,0.));
#5957=DIRECTION('center_axis',(0.,1.,0.));
#5958=DIRECTION('ref_axis',(1.,0.,0.));
#5959=DIRECTION('center_axis',(0.,-1.,0.));
#5960=DIRECTION('ref_axis',(1.,0.,0.));
#5961=DIRECTION('',(-0.707106781186547,0.707106781186548,-8.65956056235493E-17));
#5962=DIRECTION('center_axis',(0.,-1.,0.));
#5963=DIRECTION('ref_axis',(0.,0.,-1.));
#5964=DIRECTION('center_axis',(0.,-1.,0.));
#5965=DIRECTION('ref_axis',(1.,0.,0.));
#5966=DIRECTION('center_axis',(0.,1.,0.));
#5967=DIRECTION('ref_axis',(1.,0.,0.));
#5968=DIRECTION('center_axis',(0.,1.,0.));
#5969=DIRECTION('ref_axis',(1.,0.,0.));
#5970=DIRECTION('',(-0.447213595499958,0.894427190999916,-5.47678698264203E-17));
#5971=DIRECTION('center_axis',(0.,-1.,0.));
#5972=DIRECTION('ref_axis',(1.,0.,0.));
#5973=DIRECTION('',(0.,1.,0.));
#7107=CARTESIAN_POINT('',(0.,0.,0.));
#7108=CARTESIAN_POINT('Origin',(0.0866025403784439,-0.4,-0.15));
#7109=CARTESIAN_POINT('',(0.173205080756888,-0.4,0.));
#7110=CARTESIAN_POINT('',(0.0866025403784439,-0.4,-0.15));
#7111=CARTESIAN_POINT('',(0.173205080756888,-0.4,0.));
#7112=CARTESIAN_POINT('',(0.0866025403784439,-0.64,-0.15));
#7113=CARTESIAN_POINT('',(0.0866025403784439,-0.4,-0.15));
#7114=CARTESIAN_POINT('',(0.173205080756888,-0.64,0.));
#7115=CARTESIAN_POINT('',(0.173205080756888,-0.64,0.));
#7116=CARTESIAN_POINT('',(0.173205080756888,-0.4,0.));
#7117=CARTESIAN_POINT('Origin',(-0.0866025403784438,-0.4,-0.15));
#7118=CARTESIAN_POINT('',(-0.0866025403784438,-0.4,-0.15));
#7119=CARTESIAN_POINT('',(0.0866025403784439,-0.4,-0.15));
#7120=CARTESIAN_POINT('',(-0.0866025403784438,-0.64,-0.15));
#7121=CARTESIAN_POINT('',(-0.0866025403784438,-0.4,-0.15));
#7122=CARTESIAN_POINT('',(0.0866025403784439,-0.64,-0.15));
#7123=CARTESIAN_POINT('Origin',(-0.173205080756888,-0.4,-2.77555756156289E-17));
#7124=CARTESIAN_POINT('',(-0.173205080756888,-0.4,-2.12115047744981E-17));
#7125=CARTESIAN_POINT('',(-0.0866025403784438,-0.4,-0.15));
#7126=CARTESIAN_POINT('',(-0.173205080756888,-0.64,-2.77555756156289E-17));
#7127=CARTESIAN_POINT('',(-0.173205080756888,-0.4,-2.12115047744981E-17));
#7128=CARTESIAN_POINT('',(-0.0866025403784438,-0.64,-0.15));
#7129=CARTESIAN_POINT('Origin',(-0.0866025403784439,-0.4,0.15));
#7130=CARTESIAN_POINT('',(-0.0866025403784439,-0.4,0.15));
#7131=CARTESIAN_POINT('',(-0.173205080756888,-0.4,-2.12115047744981E-17));
#7132=CARTESIAN_POINT('',(-0.0866025403784439,-0.64,0.15));
#7133=CARTESIAN_POINT('',(-0.0866025403784439,-0.4,0.15));
#7134=CARTESIAN_POINT('',(-0.173205080756888,-0.64,-2.12115047744981E-17));
#7135=CARTESIAN_POINT('Origin',(0.0866025403784439,-0.4,0.15));
#7136=CARTESIAN_POINT('',(0.0866025403784439,-0.4,0.15));
#7137=CARTESIAN_POINT('',(-0.0866025403784439,-0.4,0.15));
#7138=CARTESIAN_POINT('',(0.0866025403784439,-0.64,0.15));
#7139=CARTESIAN_POINT('',(0.0866025403784439,-0.4,0.15));
#7140=CARTESIAN_POINT('',(-0.0866025403784439,-0.64,0.15));
#7141=CARTESIAN_POINT('Origin',(0.173205080756888,-0.4,0.));
#7142=CARTESIAN_POINT('',(0.0866025403784439,-0.4,0.15));
#7143=CARTESIAN_POINT('',(0.0866025403784439,-0.64,0.15));
#7144=CARTESIAN_POINT('Origin',(0.,-0.4,-2.77555756156289E-17));
#7145=CARTESIAN_POINT('Origin',(0.,-0.64,-2.77555756156289E-17));
#7146=CARTESIAN_POINT('Origin',(0.,-1.,0.));
#7147=CARTESIAN_POINT('',(-0.1954,-1.,2.39295984553393E-17));
#7148=CARTESIAN_POINT('Origin',(0.,-1.,0.));
#7149=CARTESIAN_POINT('Origin',(0.3,0.4,0.));
#7150=CARTESIAN_POINT('',(-0.3,0.4,-3.67394039744206E-17));
#7151=CARTESIAN_POINT('Origin',(0.,0.4,0.));
#7152=CARTESIAN_POINT('Origin',(0.,0.375,0.));
#7153=CARTESIAN_POINT('',(-0.35,0.35,-4.28626379701573E-17));
#7154=CARTESIAN_POINT('Origin',(0.,0.35,0.));
#7155=CARTESIAN_POINT('',(-0.325,0.375,-3.9801020972289E-17));
#7156=CARTESIAN_POINT('Origin',(0.,0.19,0.));
#7157=CARTESIAN_POINT('',(-0.35,0.03,-4.28626379701574E-17));
#7158=CARTESIAN_POINT('Origin',(0.,0.03,0.));
#7159=CARTESIAN_POINT('',(-0.35,0.19,-4.28626379701574E-17));
#7160=CARTESIAN_POINT('Origin',(0.,0.0149999999999999,0.));
#7161=CARTESIAN_POINT('',(-0.32,-3.29597460435593E-17,-3.91886975727153E-17));
#7162=CARTESIAN_POINT('Origin',(0.,0.,0.));
#7163=CARTESIAN_POINT('',(-0.335,0.0149999999999999,-4.10256677714363E-17));
#7164=CARTESIAN_POINT('Origin',(0.22,0.,0.));
#7165=CARTESIAN_POINT('',(-0.22,-6.93889390390723E-18,-2.69422295812418E-17));
#7166=CARTESIAN_POINT('Origin',(0.,0.,0.));
#7167=CARTESIAN_POINT('Origin',(0.,-0.02,0.));
#7168=CARTESIAN_POINT('',(-0.1954,-0.0492,2.39295984553393E-17));
#7169=CARTESIAN_POINT('Origin',(0.,-0.0492,0.));
#7170=CARTESIAN_POINT('',(-0.21,-0.02,-2.57175827820944E-17));
#7171=CARTESIAN_POINT('Origin',(0.,-0.8,0.));
#7172=CARTESIAN_POINT('',(-0.1954,-0.8,-2.39295984553393E-17));
#7313=UNCERTAINTY_MEASURE_WITH_UNIT(LENGTH_MEASURE(0.001),#7345,
'DISTANCE_ACCURACY_VALUE',
'Maximum model space distance between geometric entities at asserted c
onnectivities');
#7318=UNCERTAINTY_MEASURE_WITH_UNIT(LENGTH_MEASURE(0.001),#7345,
'DISTANCE_ACCURACY_VALUE',
'Maximum model space distance between geometric entities at asserted c
onnectivities');
#7339=(
GEOMETRIC_REPRESENTATION_CONTEXT(3)
GLOBAL_UNCERTAINTY_ASSIGNED_CONTEXT((#7313))
GLOBAL_UNIT_ASSIGNED_CONTEXT((#7345,#7347,#7348))
REPRESENTATION_CONTEXT('','3D')
);
#7344=(
GEOMETRIC_REPRESENTATION_CONTEXT(3)
GLOBAL_UNCERTAINTY_ASSIGNED_CONTEXT((#7318))
GLOBAL_UNIT_ASSIGNED_CONTEXT((#7345,#7347,#7348))
REPRESENTATION_CONTEXT('','3D')
);
#7345=(
LENGTH_UNIT()
NAMED_UNIT(*)
SI_UNIT(.CENTI.,.METRE.)
);
#7347=(
NAMED_UNIT(*)
PLANE_ANGLE_UNIT()
SI_UNIT($,.RADIAN.)
);
#7348=(
NAMED_UNIT(*)
SI_UNIT($,.STERADIAN.)
SOLID_ANGLE_UNIT()
);
#7369=SHAPE_DEFINITION_REPRESENTATION(#7417,#7460);
#7417=PRODUCT_DEFINITION_SHAPE('',$,#7486);
#7460=SHAPE_REPRESENTATION('',(#4769),#7339);
#7465=PRODUCT_DEFINITION_CONTEXT('part definition',#7542,'design');
#7486=PRODUCT_DEFINITION('M4x10 Cap Screw','M4x10 Cap Screw',#7511,#7465);
#7511=PRODUCT_DEFINITION_FORMATION('',$,#7564);
#7542=APPLICATION_CONTEXT(
'Core Data for Automotive Mechanical Design Process');
#7543=PRODUCT_CONTEXT('part definition',#7542,'mechanical');
#7564=PRODUCT('M4x10 Cap Screw','M4x10 Cap Screw','M4x10 Cap Screw',(#7543));
#7632=COLOUR_RGB('Black',0.12,0.14,0.17);
#7633=FILL_AREA_STYLE_COLOUR('',#7632);
#7634=FILL_AREA_STYLE('',(#7633));
#7635=SURFACE_STYLE_FILL_AREA(#7634);
#7636=SURFACE_SIDE_STYLE('',(#7635));
#7637=SURFACE_STYLE_USAGE(.BOTH.,#7636);
#7638=PRESENTATION_STYLE_ASSIGNMENT((#7637));
ENDSEC;
END-ISO-10303-21;
